ISO-10303-21;
HEADER;
/* Generated by software containing ST-Developer
 * from STEP Tools, Inc. (www.steptools.com) 
 */

FILE_DESCRIPTION(
/* description */ ('Gravity roller conveyor section'),
/* implementation_level */ '2;1');

FILE_NAME(
/* name */ 'Bonded foot pad (3).step',
/* time_stamp */ '2026-11-02T07:43:02-08:00',
/* author */ (''),
/* organization */ (''),
/* preprocessor_version */ 'ST-DEVELOPER v20.2',
/* originating_system */ 'Autodesk Translation Framework v15.17.0.0',
/* authorisation */ '');

FILE_SCHEMA (('AUTOMOTIVE_DESIGN { 1 0 10303 214 3 1 1 }'));
ENDSEC;

DATA;
#10=MECHANICAL_DESIGN_GEOMETRIC_PRESENTATION_REPRESENTATION('',(#542),#13821);
#474=SHAPE_REPRESENTATION_RELATIONSHIP('SRR','None',#14011,#508);
#508=ADVANCED_BREP_SHAPE_REPRESENTATION('',(#582),#13798);
#542=STYLED_ITEM('',(#14193),#582);
#582=MANIFOLD_SOLID_BREP('Body1',#7642);
#907=PLANE('',#8359);
#908=PLANE('',#8360);
#909=PLANE('',#8361);
#910=PLANE('',#8362);
#911=PLANE('',#8363);
#912=PLANE('',#8364);
#1246=FACE_OUTER_BOUND('',#1706,.T.);
#1247=FACE_OUTER_BOUND('',#1707,.T.);
#1248=FACE_OUTER_BOUND('',#1708,.T.);
#1249=FACE_OUTER_BOUND('',#1709,.T.);
#1250=FACE_OUTER_BOUND('',#1710,.T.);
#1251=FACE_OUTER_BOUND('',#1711,.T.);
#1706=EDGE_LOOP('',(#6438,#6439,#6440,#6441));
#1707=EDGE_LOOP('',(#6442,#6443,#6444,#6445));
#1708=EDGE_LOOP('',(#6446,#6447,#6448,#6449));
#1709=EDGE_LOOP('',(#6450,#6451,#6452,#6453));
#1710=EDGE_LOOP('',(#6454,#6455,#6456,#6457));
#1711=EDGE_LOOP('',(#6458,#6459,#6460,#6461));
#2490=LINE('',#12529,#3208);
#2491=LINE('',#12531,#3209);
#2492=LINE('',#12533,#3210);
#2493=LINE('',#12534,#3211);
#2494=LINE('',#12537,#3212);
#2495=LINE('',#12539,#3213);
#2496=LINE('',#12540,#3214);
#2497=LINE('',#12543,#3215);
#2498=LINE('',#12545,#3216);
#2499=LINE('',#12546,#3217);
#2500=LINE('',#12548,#3218);
#2501=LINE('',#12549,#3219);
#3208=VECTOR('',#9993,1.);
#3209=VECTOR('',#9994,1.);
#3210=VECTOR('',#9995,1.);
#3211=VECTOR('',#9996,1.);
#3212=VECTOR('',#9999,1.);
#3213=VECTOR('',#10000,1.);
#3214=VECTOR('',#10001,1.);
#3215=VECTOR('',#10004,1.);
#3216=VECTOR('',#10005,1.);
#3217=VECTOR('',#10006,1.);
#3218=VECTOR('',#10009,1.);
#3219=VECTOR('',#10010,1.);
#4000=VERTEX_POINT('',#12527);
#4001=VERTEX_POINT('',#12528);
#4002=VERTEX_POINT('',#12530);
#4003=VERTEX_POINT('',#12532);
#4004=VERTEX_POINT('',#12536);
#4005=VERTEX_POINT('',#12538);
#4006=VERTEX_POINT('',#12542);
#4007=VERTEX_POINT('',#12544);
#4856=EDGE_CURVE('',#4000,#4001,#2490,.T.);
#4857=EDGE_CURVE('',#4001,#4002,#2491,.T.);
#4858=EDGE_CURVE('',#4003,#4002,#2492,.T.);
#4859=EDGE_CURVE('',#4000,#4003,#2493,.T.);
#4860=EDGE_CURVE('',#4004,#4000,#2494,.T.);
#4861=EDGE_CURVE('',#4005,#4003,#2495,.T.);
#4862=EDGE_CURVE('',#4004,#4005,#2496,.T.);
#4863=EDGE_CURVE('',#4006,#4004,#2497,.T.);
#4864=EDGE_CURVE('',#4007,#4005,#2498,.T.);
#4865=EDGE_CURVE('',#4006,#4007,#2499,.T.);
#4866=EDGE_CURVE('',#4001,#4006,#2500,.T.);
#4867=EDGE_CURVE('',#4002,#4007,#2501,.T.);
#6438=ORIENTED_EDGE('',*,*,#4856,.T.);
#6439=ORIENTED_EDGE('',*,*,#4857,.T.);
#6440=ORIENTED_EDGE('',*,*,#4858,.F.);
#6441=ORIENTED_EDGE('',*,*,#4859,.F.);
#6442=ORIENTED_EDGE('',*,*,#4860,.T.);
#6443=ORIENTED_EDGE('',*,*,#4859,.T.);
#6444=ORIENTED_EDGE('',*,*,#4861,.F.);
#6445=ORIENTED_EDGE('',*,*,#4862,.F.);
#6446=ORIENTED_EDGE('',*,*,#4863,.T.);
#6447=ORIENTED_EDGE('',*,*,#4862,.T.);
#6448=ORIENTED_EDGE('',*,*,#4864,.F.);
#6449=ORIENTED_EDGE('',*,*,#4865,.F.);
#6450=ORIENTED_EDGE('',*,*,#4866,.T.);
#6451=ORIENTED_EDGE('',*,*,#4865,.T.);
#6452=ORIENTED_EDGE('',*,*,#4867,.F.);
#6453=ORIENTED_EDGE('',*,*,#4857,.F.);
#6454=ORIENTED_EDGE('',*,*,#4867,.T.);
#6455=ORIENTED_EDGE('',*,*,#4864,.T.);
#6456=ORIENTED_EDGE('',*,*,#4861,.T.);
#6457=ORIENTED_EDGE('',*,*,#4858,.T.);
#6458=ORIENTED_EDGE('',*,*,#4866,.F.);
#6459=ORIENTED_EDGE('',*,*,#4856,.F.);
#6460=ORIENTED_EDGE('',*,*,#4860,.F.);
#6461=ORIENTED_EDGE('',*,*,#4863,.F.);
#7447=ADVANCED_FACE('',(#1246),#907,.T.);
#7448=ADVANCED_FACE('',(#1247),#908,.T.);
#7449=ADVANCED_FACE('',(#1248),#909,.T.);
#7450=ADVANCED_FACE('',(#1249),#910,.T.);
#7451=ADVANCED_FACE('',(#1250),#911,.T.);
#7452=ADVANCED_FACE('',(#1251),#912,.F.);
#7642=CLOSED_SHELL('',(#7447,#7448,#7449,#7450,#7451,#7452));
#8358=AXIS2_PLACEMENT_3D('',#12525,#9989,#9990);
#8359=AXIS2_PLACEMENT_3D('',#12526,#9991,#9992);
#8360=AXIS2_PLACEMENT_3D('',#12535,#9997,#9998);
#8361=AXIS2_PLACEMENT_3D('',#12541,#10002,#10003);
#8362=AXIS2_PLACEMENT_3D('',#12547,#10007,#10008);
#8363=AXIS2_PLACEMENT_3D('',#12550,#10011,#10012);
#8364=AXIS2_PLACEMENT_3D('',#12551,#10013,#10014);
#9989=DIRECTION('axis',(0.,0.,1.));
#9990=DIRECTION('refdir',(1.,0.,0.));
#9991=DIRECTION('center_axis',(0.,1.,0.));
#9992=DIRECTION('ref_axis',(-1.,0.,0.));
#9993=DIRECTION('',(-1.,0.,0.));
#9994=DIRECTION('',(0.,0.,1.));
#9995=DIRECTION('',(-1.,0.,0.));
#9996=DIRECTION('',(0.,0.,1.));
#9997=DIRECTION('center_axis',(1.,0.,0.));
#9998=DIRECTION('ref_axis',(0.,1.,0.));
#9999=DIRECTION('',(0.,1.,0.));
#10000=DIRECTION('',(0.,1.,0.));
#10001=DIRECTION('',(0.,0.,1.));
#10002=DIRECTION('center_axis',(0.,-1.,0.));
#10003=DIRECTION('ref_axis',(1.,0.,0.));
#10004=DIRECTION('',(1.,0.,0.));
#10005=DIRECTION('',(1.,0.,0.));
#10006=DIRECTION('',(0.,0.,1.));
#10007=DIRECTION('center_axis',(-1.,0.,0.));
#10008=DIRECTION('ref_axis',(0.,-1.,0.));
#10009=DIRECTION('',(0.,-1.,0.));
#10010=DIRECTION('',(0.,-1.,0.));
#10011=DIRECTION('center_axis',(0.,0.,1.));
#10012=DIRECTION('ref_axis',(1.,0.,0.));
#10013=DIRECTION('center_axis',(0.,0.,1.));
#10014=DIRECTION('ref_axis',(1.,0.,0.));
#12525=CARTESIAN_POINT('',(0.,0.,0.));
#12526=CARTESIAN_POINT('Origin',(56.,35.,-17.6));
#12527=CARTESIAN_POINT('',(56.,35.,-17.6));
#12528=CARTESIAN_POINT('',(52.,35.,-17.6));
#12529=CARTESIAN_POINT('',(56.,35.,-17.6));
#12530=CARTESIAN_POINT('',(52.,35.,-16.8));
#12531=CARTESIAN_POINT('',(52.,35.,-17.6));
#12532=CARTESIAN_POINT('',(56.,35.,-16.8));
#12533=CARTESIAN_POINT('',(56.,35.,-16.8));
#12534=CARTESIAN_POINT('',(56.,35.,-17.6));
#12535=CARTESIAN_POINT('Origin',(56.,33.5,-17.6));
#12536=CARTESIAN_POINT('',(56.,33.5,-17.6));
#12537=CARTESIAN_POINT('',(56.,33.5,-17.6));
#12538=CARTESIAN_POINT('',(56.,33.5,-16.8));
#12539=CARTESIAN_POINT('',(56.,33.5,-16.8));
#12540=CARTESIAN_POINT('',(56.,33.5,-17.6));
#12541=CARTESIAN_POINT('Origin',(52.,33.5,-17.6));
#12542=CARTESIAN_POINT('',(52.,33.5,-17.6));
#12543=CARTESIAN_POINT('',(52.,33.5,-17.6));
#12544=CARTESIAN_POINT('',(52.,33.5,-16.8));
#12545=CARTESIAN_POINT('',(52.,33.5,-16.8));
#12546=CARTESIAN_POINT('',(52.,33.5,-17.6));
#12547=CARTESIAN_POINT('Origin',(52.,35.,-17.6));
#12548=CARTESIAN_POINT('',(52.,35.,-17.6));
#12549=CARTESIAN_POINT('',(52.,35.,-16.8));
#12550=CARTESIAN_POINT('Origin',(54.,34.25,-16.8));
#12551=CARTESIAN_POINT('Origin',(54.,34.25,-17.6));
#13759=UNCERTAINTY_MEASURE_WITH_UNIT(LENGTH_MEASURE(0.001),#13822,
'DISTANCE_ACCURACY_VALUE',
'Maximum model space distance between geometric entities at asserted c
onnectivities');
#13782=UNCERTAINTY_MEASURE_WITH_UNIT(LENGTH_MEASURE(0.001),#13822,
'DISTANCE_ACCURACY_VALUE',
'Maximum model space distance between geometric entities at asserted c
onnectivities');
#13798=(
GEOMETRIC_REPRESENTATION_CONTEXT(3)
GLOBAL_UNCERTAINTY_ASSIGNED_CONTEXT((#13759))
GLOBAL_UNIT_ASSIGNED_CONTEXT((#13822,#13824,#13825))
REPRESENTATION_CONTEXT('','3D')
);
#13821=(
GEOMETRIC_REPRESENTATION_CONTEXT(3)
GLOBAL_UNCERTAINTY_ASSIGNED_CONTEXT((#13782))
GLOBAL_UNIT_ASSIGNED_CONTEXT((#13822,#13824,#13825))
REPRESENTATION_CONTEXT('','3D')
);
#13822=(
LENGTH_UNIT()
NAMED_UNIT(*)
SI_UNIT(.CENTI.,.METRE.)
);
#13824=(
NAMED_UNIT(*)
PLANE_ANGLE_UNIT()
SI_UNIT($,.RADIAN.)
);
#13825=(
NAMED_UNIT(*)
SI_UNIT($,.STERADIAN.)
SOLID_ANGLE_UNIT()
);
#13841=SHAPE_DEFINITION_REPRESENTATION(#13879,#14011);
#13879=PRODUCT_DEFINITION_SHAPE('',$,#14050);
#14011=SHAPE_REPRESENTATION('',(#8358),#13798);
#14034=PRODUCT_DEFINITION_CONTEXT('part definition',#14150,'design');
#14050=PRODUCT_DEFINITION('Bonded foot pad_3','Bonded foot pad (3)',#14088,
#14034);
#14088=PRODUCT_DEFINITION_FORMATION('',$,#14167);
#14150=APPLICATION_CONTEXT(
'Core Data for Automotive Mechanical Design Process');
#14151=PRODUCT_CONTEXT('part definition',#14150,'mechanical');
#14167=PRODUCT('Bonded foot pad_3','Bonded foot pad (3)',
'Bonded foot pad',(#14151));
#14193=PRESENTATION_STYLE_ASSIGNMENT((#14198));
#14198=SURFACE_STYLE_USAGE(.BOTH.,#14203);
#14203=SURFACE_SIDE_STYLE('',(#14208));
#14208=SURFACE_STYLE_FILL_AREA(#14213);
#14213=FILL_AREA_STYLE('CAD Library Painted - Graphite',(#14218));
#14218=FILL_AREA_STYLE_COLOUR('CAD Library Painted - Graphite',#14223);
#14223=COLOUR_RGB('CAD Library Painted - Graphite',0.168627450980392,0.192156862745098,
0.231372549019608);
ENDSEC;
END-ISO-10303-21;
